ISO-10303-21;
HEADER;
FILE_DESCRIPTION (('STEP AP214'),
    '1' );
FILE_NAME ('Bolt1.step',
    '2026-10-28T16:39:03',
    ( '' ),
    ( '' ),
    'SwSTEP 2.0',
    'SolidWorks 2024',
    '' );
FILE_SCHEMA (( 'AUTOMOTIVE_DESIGN' ));
ENDSEC;

DATA;
#17=ORIENTED_EDGE ( 'NONE', *, *, #7884, .F. ) ;
#152=ORIENTED_EDGE ( 'NONE', *, *, #6160, .T. ) ;
#189=DIRECTION ( 'NONE',  ( 1.000000000000000000, 0.000000000000000000, 0.000000000000000000 ) ) ;
#213=DIRECTION ( 'NONE',  ( 0.000000000000000000, 0.000000000000000000, 1.000000000000000000 ) ) ;
#243=VERTEX_POINT ( 'NONE', #7446 ) ;
#246=CARTESIAN_POINT ( 'NONE',  ( 0.000000000000000000, 0.000000000000000000, 47.50000000000000000 ) ) ;
#267=CARTESIAN_POINT ( 'NONE',  ( -15.00000000000000000, 2.143131898507867854E-15, 52.50000000000000000 ) ) ;
#282=DIRECTION ( 'NONE',  ( 0.000000000000000000, 0.000000000000000000, 1.000000000000000000 ) ) ;
#286=DIRECTION ( 'NONE',  ( 1.000000000000000000, 0.000000000000000000, 0.000000000000000000 ) ) ;
#335=( NAMED_UNIT ( * ) PLANE_ANGLE_UNIT ( ) SI_UNIT ( $, .RADIAN. ) );
#348=AXIS2_PLACEMENT_3D ( 'NONE', #7549, #7663, #286 ) ;
#352=AXIS2_PLACEMENT_3D ( 'NONE', #7309, #4972, #1287 ) ;
#355=ORIENTED_EDGE ( 'NONE', *, *, #2109, .F. ) ;
#386=UNCERTAINTY_MEASURE_WITH_UNIT (LENGTH_MEASURE( 1.000000000000000082E-05 ), #2222, 'distance_accuracy_value', 'NONE');
#398=VECTOR ( 'NONE', #6962, 1000.000000000000114 ) ;
#443=VERTEX_POINT ( 'NONE', #979 ) ;
#519=CYLINDRICAL_SURFACE ( 'NONE', #5579, 12.50000000000000000 ) ;
#606=MECHANICAL_DESIGN_GEOMETRIC_PRESENTATION_REPRESENTATION('',(#4056),#729);
#607=ORIENTED_EDGE ( 'NONE', *, *, #3175, .F. ) ;
#680=EDGE_LOOP ( 'NONE', ( #1068, #3296 ) ) ;
#712=CARTESIAN_POINT ( 'NONE',  ( 0.000000000000000000, 0.000000000000000000, 1.000000000000028644 ) ) ;
#729=( GEOMETRIC_REPRESENTATION_CONTEXT ( 3 ) GLOBAL_UNCERTAINTY_ASSIGNED_CONTEXT ( ( #386 ) ) GLOBAL_UNIT_ASSIGNED_CONTEXT ( ( #2222, #335, #7676 ) ) REPRESENTATION_CONTEXT ( 'NONE', 'WORKASPACE' ) );
#731=LINE ( 'NONE', #7435, #7643 ) ;
#755=CARTESIAN_POINT ( 'NONE',  ( 11.49999999999995914, 0.000000000000000000, 0.000000000000000000 ) ) ;
#757=AXIS2_PLACEMENT_3D ( 'NONE', #1518, #3404, #5810 ) ;
#825=CARTESIAN_POINT ( 'NONE',  ( -12.50000000000000000, 1.530808498934191521E-15, 1.000000000000028644 ) ) ;
#839=EDGE_LOOP ( 'NONE', ( #5596, #2921, #2429, #1231 ) ) ;
#845=CONICAL_SURFACE ( 'NONE', #5330, 12.50000000000000000, 0.7853981633974543852 ) ;
#877=AXIS2_PLACEMENT_3D ( 'NONE', #4636, #3286, #1593 ) ;
#878=AXIS2_PLACEMENT_3D ( 'NONE', #7202, #7715, #1699 ) ;
#955=EDGE_LOOP ( 'NONE', ( #17, #3274, #1865, #4677 ) ) ;
#979=CARTESIAN_POINT ( 'NONE',  ( -20.00000000000000000, 0.000000000000000000, 47.50000000000000000 ) ) ;
#1024=CARTESIAN_POINT ( 'NONE',  ( 0.000000000000000000, 0.000000000000000000, 47.50000000000000000 ) ) ;
#1058=ADVANCED_FACE ( 'NONE', ( #4733 ), #1090, .T. ) ;
#1068=ORIENTED_EDGE ( 'NONE', *, *, #4674, .T. ) ;
#1090=PLANE ( 'NONE',  #1469 ) ;
#1110=FACE_OUTER_BOUND ( 'NONE', #4157, .T. ) ;
#1128=DIRECTION ( 'NONE',  ( 0.000000000000000000, 0.000000000000000000, 1.000000000000000000 ) ) ;
#1131=AXIS2_PLACEMENT_3D ( 'NONE', #2016, #213, #1495 ) ;
#1188=EDGE_LOOP ( 'NONE', ( #3811, #2086 ) ) ;
#1231=ORIENTED_EDGE ( 'NONE', *, *, #5161, .F. ) ;
#1246=DIRECTION ( 'NONE',  ( 1.000000000000000000, 0.000000000000000000, 0.000000000000000000 ) ) ;
#1251=FACE_OUTER_BOUND ( 'NONE', #955, .T. ) ;
#1287=DIRECTION ( 'NONE',  ( 1.000000000000000000, 0.000000000000000000, -0.000000000000000000 ) ) ;
#1294=PRODUCT_DEFINITION ( 'UNKNOWN', '', #4114, #7124 ) ;
#1307=CARTESIAN_POINT ( 'NONE',  ( 12.50000000000000000, 0.000000000000000000, 1.000000000000028644 ) ) ;
#1309=EDGE_CURVE ( 'NONE', #7297, #6889, #2084, .T. ) ;
#1391=ADVANCED_FACE ( 'NONE', ( #2650 ), #6375, .F. ) ;
#1395=ADVANCED_FACE ( 'NONE', ( #2043 ), #4916, .T. ) ;
#1431=CARTESIAN_POINT ( 'NONE',  ( 0.000000000000000000, 0.000000000000000000, 47.50000000000000000 ) ) ;
#1469=AXIS2_PLACEMENT_3D ( 'NONE', #5254, #1128, #3421 ) ;
#1481=CARTESIAN_POINT ( 'NONE',  ( 0.000000000000000000, 0.000000000000000000, 45.00000000000000000 ) ) ;
#1494=CIRCLE ( 'NONE', #348, 11.49999999999995914 ) ;
#1495=DIRECTION ( 'NONE',  ( 1.000000000000000000, 0.000000000000000000, 0.000000000000000000 ) ) ;
#1518=CARTESIAN_POINT ( 'NONE',  ( 0.000000000000000000, 0.000000000000000000, 52.50000000000000000 ) ) ;
#1530=CIRCLE ( 'NONE', #4722, 4.999999999999997335 ) ;
#1588=CONICAL_SURFACE ( 'NONE', #1844, 12.50000000000000000, 0.7853981633974543852 ) ;
#1593=DIRECTION ( 'NONE',  ( 1.000000000000000000, 0.000000000000000000, 0.000000000000000000 ) ) ;
#1600=EDGE_CURVE ( 'NONE', #2808, #243, #6882, .T. ) ;
#1609=DIRECTION ( 'NONE',  ( -0.000000000000000000, -0.000000000000000000, -1.000000000000000000 ) ) ;
#1614=AXIS2_PLACEMENT_3D ( 'NONE', #5846, #7129, #1628 ) ;
#1628=DIRECTION ( 'NONE',  ( 1.000000000000000000, 0.000000000000000000, 0.000000000000000000 ) ) ;
#1676=DIRECTION ( 'NONE',  ( -0.000000000000000000, -0.000000000000000000, -1.000000000000000000 ) ) ;
#1699=DIRECTION ( 'NONE',  ( 1.000000000000000000, 0.000000000000000000, 0.000000000000000000 ) ) ;
#1733=PRODUCT_CONTEXT ( 'NONE', #2591, 'mechanical' ) ;
#1746=ORIENTED_EDGE ( 'NONE', *, *, #5161, .T. ) ;
#1765=DIRECTION ( 'NONE',  ( 0.000000000000000000, 0.000000000000000000, 1.000000000000000000 ) ) ;
#1772=SHAPE_REPRESENTATION ( 'Bolt1', ( #5785 ), #1803 ) ;
#1803=( GEOMETRIC_REPRESENTATION_CONTEXT ( 3 ) GLOBAL_UNCERTAINTY_ASSIGNED_CONTEXT ( ( #4469 ) ) GLOBAL_UNIT_ASSIGNED_CONTEXT ( ( #1858, #6799, #4304 ) ) REPRESENTATION_CONTEXT ( 'NONE', 'WORKASPACE' ) );
#1844=AXIS2_PLACEMENT_3D ( 'NONE', #3707, #6301, #5541 ) ;
#1847=CIRCLE ( 'NONE', #3019, 11.49999999999995914 ) ;
#1856=ORIENTED_EDGE ( 'NONE', *, *, #4990, .F. ) ;
#1858=( LENGTH_UNIT ( ) NAMED_UNIT ( * ) SI_UNIT ( .MILLI., .METRE. ) );
#1865=ORIENTED_EDGE ( 'NONE', *, *, #1600, .T. ) ;
#1879=ORIENTED_EDGE ( 'NONE', *, *, #2482, .T. ) ;
#1882=PLANE ( 'NONE',  #352 ) ;
#1899=EDGE_LOOP ( 'NONE', ( #2834, #4073, #1856, #4123 ) ) ;
#2005=CARTESIAN_POINT ( 'NONE',  ( -12.50000000000000000, 0.000000000000000000, 45.00000000000000000 ) ) ;
#2016=CARTESIAN_POINT ( 'NONE',  ( 0.000000000000000000, 0.000000000000000000, 45.00000000000000000 ) ) ;
#2032=CIRCLE ( 'NONE', #877, 12.50000000000000000 ) ;
#2039=DIRECTION ( 'NONE',  ( -1.000000000000000000, 0.000000000000000000, 0.000000000000000000 ) ) ;
#2043=FACE_OUTER_BOUND ( 'NONE', #4879, .T. ) ;
#2084=CIRCLE ( 'NONE', #6313, 20.00000000000000000 ) ;
#2086=ORIENTED_EDGE ( 'NONE', *, *, #3997, .T. ) ;
#2109=EDGE_CURVE ( 'NONE', #2387, #3363, #5907, .T. ) ;
#2115=FACE_OUTER_BOUND ( 'NONE', #4804, .T. ) ;
#2177=CARTESIAN_POINT ( 'NONE',  ( -11.49999999999995914, 1.469576158976821383E-15, 0.000000000000000000 ) ) ;
#2222=( LENGTH_UNIT ( ) NAMED_UNIT ( * ) SI_UNIT ( .MILLI., .METRE. ) );
#2252=DIRECTION ( 'NONE',  ( -0.000000000000000000, -0.000000000000000000, -1.000000000000000000 ) ) ;
#2256=ORIENTED_EDGE ( 'NONE', *, *, #3175, .T. ) ;
#2322=CARTESIAN_POINT ( 'NONE',  ( 0.000000000000000000, 0.000000000000000000, 47.50000000000000000 ) ) ;
#2351=DIRECTION ( 'NONE',  ( 1.000000000000000000, 0.000000000000000000, 0.000000000000000000 ) ) ;
#2387=VERTEX_POINT ( 'NONE', #2005 ) ;
#2429=ORIENTED_EDGE ( 'NONE', *, *, #1309, .T. ) ;
#2430=ADVANCED_FACE ( 'NONE', ( #1251 ), #1588, .T. ) ;
#2452=FACE_BOUND ( 'NONE', #4509, .T. ) ;
#2480=CLOSED_SHELL ( 'NONE', ( #3764, #7533, #7385, #6698, #3262, #1391, #7578, #1058, #5019, #1395, #2430 ) ) ;
#2482=EDGE_CURVE ( 'NONE', #243, #3363, #7609, .T. ) ;
#2535=AXIS2_PLACEMENT_3D ( 'NONE', #6456, #2252, #7061 ) ;
#2571=DIRECTION ( 'NONE',  ( -0.000000000000000000, -0.000000000000000000, 1.000000000000000000 ) ) ;
#2591=APPLICATION_CONTEXT ( 'automotive_design' ) ;
#2610=VECTOR ( 'NONE', #1609, 1000.000000000000000 ) ;
#2617=AXIS2_PLACEMENT_3D ( 'NONE', #3183, #2571, #5014 ) ;
#2650=FACE_OUTER_BOUND ( 'NONE', #680, .T. ) ;
#2722=ORIENTED_EDGE ( 'NONE', *, *, #7621, .F. ) ;
#2754=ORIENTED_EDGE ( 'NONE', *, *, #7145, .T. ) ;
#2769=CARTESIAN_POINT ( 'NONE',  ( 12.50000000000000000, 1.530808498934191127E-15, 45.00000000000000000 ) ) ;
#2776=PRODUCT ( 'Bolt1', 'Bolt1', '', ( #1733 ) ) ;
#2807=DIRECTION ( 'NONE',  ( 0.000000000000000000, 0.000000000000000000, 1.000000000000000000 ) ) ;
#2808=VERTEX_POINT ( 'NONE', #755 ) ;
#2834=ORIENTED_EDGE ( 'NONE', *, *, #5816, .F. ) ;
#2883=AXIS2_PLACEMENT_3D ( 'NONE', #3334, #7543, #6977 ) ;
#2898=ORIENTED_EDGE ( 'NONE', *, *, #5147, .F. ) ;
#2914=DIRECTION ( 'NONE',  ( 1.000000000000000000, 0.000000000000000000, 0.000000000000000000 ) ) ;
#2921=ORIENTED_EDGE ( 'NONE', *, *, #4528, .T. ) ;
#2934=CIRCLE ( 'NONE', #1131, 20.00000000000000000 ) ;
#2999=EDGE_CURVE ( 'NONE', #7266, #2808, #1847, .T. ) ;
#3019=AXIS2_PLACEMENT_3D ( 'NONE', #3242, #5692, #189 ) ;
#3038=SHAPE_REPRESENTATION_RELATIONSHIP ( 'NONE' , 'NONE' ,  #1772, #4490 ) ;
#3121=DIRECTION ( 'NONE',  ( -0.000000000000000000, -0.000000000000000000, -1.000000000000000000 ) ) ;
#3175=EDGE_CURVE ( 'NONE', #5938, #443, #4295, .T. ) ;
#3181=VECTOR ( 'NONE', #5044, 1000.000000000000000 ) ;
#3183=CARTESIAN_POINT ( 'NONE',  ( 0.000000000000000000, 0.000000000000000000, 1.000000000000028644 ) ) ;
#3192=AXIS2_PLACEMENT_3D ( 'NONE', #1431, #2807, #7649 ) ;
#3242=CARTESIAN_POINT ( 'NONE',  ( 0.000000000000000000, 0.000000000000000000, 0.000000000000000000 ) ) ;
#3262=ADVANCED_FACE ( 'NONE', ( #1110 ), #519, .T. ) ;
#3263=VECTOR ( 'NONE', #5645, 1000.000000000000114 ) ;
#3274=ORIENTED_EDGE ( 'NONE', *, *, #4674, .F. ) ;
#3286=DIRECTION ( 'NONE',  ( -0.000000000000000000, -0.000000000000000000, 1.000000000000000000 ) ) ;
#3296=ORIENTED_EDGE ( 'NONE', *, *, #2999, .T. ) ;
#3306=ORIENTED_EDGE ( 'NONE', *, *, #4528, .F. ) ;
#3313=EDGE_LOOP ( 'NONE', ( #7815, #4023, #4842, #3329 ) ) ;
#3321=DIRECTION ( 'NONE',  ( -0.000000000000000000, -0.000000000000000000, -1.000000000000000000 ) ) ;
#3329=ORIENTED_EDGE ( 'NONE', *, *, #1600, .F. ) ;
#3334=CARTESIAN_POINT ( 'NONE',  ( 0.000000000000000000, 0.000000000000000000, 0.000000000000000000 ) ) ;
#3354=ORIENTED_EDGE ( 'NONE', *, *, #5784, .F. ) ;
#3363=VERTEX_POINT ( 'NONE', #6127 ) ;
#3404=DIRECTION ( 'NONE',  ( -0.000000000000000000, -0.000000000000000000, -1.000000000000000000 ) ) ;
#3421=DIRECTION ( 'NONE',  ( 1.000000000000000000, 0.000000000000000000, -0.000000000000000000 ) ) ;
#3422=CARTESIAN_POINT ( 'NONE',  ( -12.50000000000000000, 0.000000000000000000, 45.00000000000000000 ) ) ;
#3566=CARTESIAN_POINT ( 'NONE',  ( 0.000000000000000000, 0.000000000000000000, 45.00000000000000000 ) ) ;
#3567=EDGE_LOOP ( 'NONE', ( #7018, #6372 ) ) ;
#3571=FACE_OUTER_BOUND ( 'NONE', #6042, .T. ) ;
#3587=SHAPE_DEFINITION_REPRESENTATION ( #6290, #1772 ) ;
#3665=AXIS2_PLACEMENT_3D ( 'NONE', #2322, #1676, #4078 ) ;
#3671=CARTESIAN_POINT ( 'NONE',  ( 20.00000000000000000, 2.449293598294706513E-15, 47.50000000000000000 ) ) ;
#3707=CARTESIAN_POINT ( 'NONE',  ( 0.000000000000000000, 0.000000000000000000, 1.000000000000028644 ) ) ;
#3731=APPLICATION_CONTEXT ( 'automotive_design' ) ;
#3742=ORIENTED_EDGE ( 'NONE', *, *, #3843, .F. ) ;
#3764=ADVANCED_FACE ( 'NONE', ( #3768 ), #845, .T. ) ;
#3768=FACE_OUTER_BOUND ( 'NONE', #3313, .T. ) ;
#3775=DIRECTION ( 'NONE',  ( 1.224646799147353207E-16, 1.000000000000000000, -0.000000000000000000 ) ) ;
#3811=ORIENTED_EDGE ( 'NONE', *, *, #4990, .T. ) ;
#3813=CARTESIAN_POINT ( 'NONE',  ( -20.00000000000000000, 0.000000000000000000, 52.50000000000000000 ) ) ;
#3843=EDGE_CURVE ( 'NONE', #5237, #243, #4389, .T. ) ;
#3923=CIRCLE ( 'NONE', #1614, 15.00000000000000000 ) ;
#3997=EDGE_CURVE ( 'NONE', #7839, #7303, #3923, .T. ) ;
#4023=ORIENTED_EDGE ( 'NONE', *, *, #7884, .T. ) ;
#4056=STYLED_ITEM('',(#7969),#4352);
#4073=ORIENTED_EDGE ( 'NONE', *, *, #5147, .T. ) ;
#4078=DIRECTION ( 'NONE',  ( 1.000000000000000000, 0.000000000000000000, 0.000000000000000000 ) ) ;
#4099=CARTESIAN_POINT ( 'NONE',  ( 20.00000000000000000, 2.449293598294706513E-15, 45.00000000000000000 ) ) ;
#4110=CARTESIAN_POINT ( 'NONE',  ( 0.000000000000000000, 0.000000000000000000, 0.000000000000000000 ) ) ;
#4114=PRODUCT_DEFINITION_FORMATION_WITH_SPECIFIED_SOURCE ( 'ANY', '', #2776, .NOT_KNOWN. ) ;
#4123=ORIENTED_EDGE ( 'NONE', *, *, #6160, .F. ) ;
#4157=EDGE_LOOP ( 'NONE', ( #3742, #2722, #5549, #6059 ) ) ;
#4186=DIRECTION ( 'NONE',  ( 0.000000000000000000, 0.000000000000000000, 1.000000000000000000 ) ) ;
#4295=CIRCLE ( 'NONE', #3665, 20.00000000000000000 ) ;
#4304=( NAMED_UNIT ( * ) SI_UNIT ( $, .STERADIAN. ) SOLID_ANGLE_UNIT ( ) );
#4320=CIRCLE ( 'NONE', #7904, 15.00000000000000000 ) ;
#4352=MANIFOLD_SOLID_BREP ( 'Pah1', #2480 ) ;
#4384=DIRECTION ( 'NONE',  ( -1.000000000000000000, 0.000000000000000000, 0.000000000000000000 ) ) ;
#4389=LINE ( 'NONE', #6852, #5972 ) ;
#4469=UNCERTAINTY_MEASURE_WITH_UNIT (LENGTH_MEASURE( 1.000000000000000082E-05 ), #1858, 'distance_accuracy_value', 'NONE');
#4490=ADVANCED_BREP_SHAPE_REPRESENTATION ( '', ( #4352, #5785 ), #1803 ) ;
#4509=EDGE_LOOP ( 'NONE', ( #7123, #7777 ) ) ;
#4528=EDGE_CURVE ( 'NONE', #5938, #7297, #731, .T. ) ;
#4551=LINE ( 'NONE', #825, #398 ) ;
#4555=CARTESIAN_POINT ( 'NONE',  ( -20.00000000000000000, 0.000000000000000000, 45.00000000000000000 ) ) ;
#4560=CYLINDRICAL_SURFACE ( 'NONE', #757, 20.00000000000000000 ) ;
#4564=DIRECTION ( 'NONE',  ( 0.000000000000000000, 0.000000000000000000, 1.000000000000000000 ) ) ;
#4583=AXIS2_PLACEMENT_3D ( 'NONE', #1024, #5305, #2914 ) ;
#4636=CARTESIAN_POINT ( 'NONE',  ( 0.000000000000000000, 0.000000000000000000, 1.000000000000028644 ) ) ;
#4674=EDGE_CURVE ( 'NONE', #2808, #7266, #1494, .T. ) ;
#4677=ORIENTED_EDGE ( 'NONE', *, *, #7449, .F. ) ;
#4717=DIRECTION ( 'NONE',  ( 0.000000000000000000, 0.000000000000000000, 1.000000000000000000 ) ) ;
#4722=AXIS2_PLACEMENT_3D ( 'NONE', #5667, #6625, #7859 ) ;
#4733=FACE_OUTER_BOUND ( 'NONE', #1188, .T. ) ;
#4804=EDGE_LOOP ( 'NONE', ( #3306, #2256, #1746, #2754 ) ) ;
#4842=ORIENTED_EDGE ( 'NONE', *, *, #2482, .F. ) ;
#4879=EDGE_LOOP ( 'NONE', ( #2898, #607, #152, #7895 ) ) ;
#4895=CYLINDRICAL_SURFACE ( 'NONE', #4977, 20.00000000000000000 ) ;
#4916=TOROIDAL_SURFACE ( 'NONE', #7229, 15.00000000000000000, 5.000000000000000000 ) ;
#4972=DIRECTION ( 'NONE',  ( 0.000000000000000000, 0.000000000000000000, 1.000000000000000000 ) ) ;
#4977=AXIS2_PLACEMENT_3D ( 'NONE', #6671, #7352, #2039 ) ;
#4990=EDGE_CURVE ( 'NONE', #7303, #7839, #4320, .T. ) ;
#5014=DIRECTION ( 'NONE',  ( 1.000000000000000000, 0.000000000000000000, 0.000000000000000000 ) ) ;
#5015=DIRECTION ( 'NONE',  ( -0.000000000000000000, -0.000000000000000000, -1.000000000000000000 ) ) ;
#5019=ADVANCED_FACE ( 'NONE', ( #2452, #7387 ), #1882, .F. ) ;
#5041=FACE_OUTER_BOUND ( 'NONE', #839, .T. ) ;
#5044=DIRECTION ( 'NONE',  ( -0.000000000000000000, -0.000000000000000000, -1.000000000000000000 ) ) ;
#5123=DIRECTION ( 'NONE',  ( -1.000000000000000000, 1.224646799147353454E-16, 0.000000000000000000 ) ) ;
#5147=EDGE_CURVE ( 'NONE', #443, #7839, #5608, .T. ) ;
#5161=EDGE_CURVE ( 'NONE', #443, #6889, #6863, .T. ) ;
#5223=CIRCLE ( 'NONE', #4583, 20.00000000000000000 ) ;
#5237=VERTEX_POINT ( 'NONE', #2769 ) ;
#5254=CARTESIAN_POINT ( 'NONE',  ( 0.000000000000000000, 0.000000000000000000, 52.50000000000000000 ) ) ;
#5305=DIRECTION ( 'NONE',  ( -0.000000000000000000, -0.000000000000000000, -1.000000000000000000 ) ) ;
#5330=AXIS2_PLACEMENT_3D ( 'NONE', #712, #5687, #5611 ) ;
#5501=CARTESIAN_POINT ( 'NONE',  ( 0.000000000000000000, 0.000000000000000000, 52.50000000000000000 ) ) ;
#5541=DIRECTION ( 'NONE',  ( 1.000000000000000000, 0.000000000000000000, 0.000000000000000000 ) ) ;
#5543=CARTESIAN_POINT ( 'NONE',  ( 15.00000000000000000, 0.000000000000000000, 52.50000000000000000 ) ) ;
#5549=ORIENTED_EDGE ( 'NONE', *, *, #2109, .T. ) ;
#5579=AXIS2_PLACEMENT_3D ( 'NONE', #6843, #3121, #4384 ) ;
#5596=ORIENTED_EDGE ( 'NONE', *, *, #5816, .T. ) ;
#5608=CIRCLE ( 'NONE', #7014, 5.000000000000000888 ) ;
#5611=DIRECTION ( 'NONE',  ( 1.000000000000000000, 0.000000000000000000, 0.000000000000000000 ) ) ;
#5632=CIRCLE ( 'NONE', #5889, 12.50000000000000000 ) ;
#5645=DIRECTION ( 'NONE',  ( 0.7071067811865517916, 0.000000000000000000, 0.7071067811865431318 ) ) ;
#5667=CARTESIAN_POINT ( 'NONE',  ( 15.00000000000000000, 0.000000000000000000, 47.50000000000000000 ) ) ;
#5687=DIRECTION ( 'NONE',  ( -0.000000000000000000, -0.000000000000000000, 1.000000000000000000 ) ) ;
#5692=DIRECTION ( 'NONE',  ( -0.000000000000000000, -0.000000000000000000, -1.000000000000000000 ) ) ;
#5739=CARTESIAN_POINT ( 'NONE',  ( -15.00000000000000000, 1.836970198721029589E-15, 47.50000000000000000 ) ) ;
#5784=EDGE_CURVE ( 'NONE', #5237, #2387, #6902, .T. ) ;
#5785=AXIS2_PLACEMENT_3D ( 'NONE', #4110, #4186, #2351 ) ;
#5810=DIRECTION ( 'NONE',  ( -1.000000000000000000, 0.000000000000000000, 0.000000000000000000 ) ) ;
#5816=EDGE_CURVE ( 'NONE', #443, #5938, #5223, .T. ) ;
#5843=ORIENTED_EDGE ( 'NONE', *, *, #3843, .T. ) ;
#5846=CARTESIAN_POINT ( 'NONE',  ( 0.000000000000000000, 0.000000000000000000, 52.50000000000000000 ) ) ;
#5889=AXIS2_PLACEMENT_3D ( 'NONE', #3566, #4717, #6014 ) ;
#5907=LINE ( 'NONE', #3422, #2610 ) ;
#5938=VERTEX_POINT ( 'NONE', #3671 ) ;
#5972=VECTOR ( 'NONE', #3321, 1000.000000000000000 ) ;
#6014=DIRECTION ( 'NONE',  ( 1.000000000000000000, 0.000000000000000000, 0.000000000000000000 ) ) ;
#6020=CYLINDRICAL_SURFACE ( 'NONE', #2535, 12.50000000000000000 ) ;
#6042=EDGE_LOOP ( 'NONE', ( #3354, #5843, #1879, #355 ) ) ;
#6059=ORIENTED_EDGE ( 'NONE', *, *, #7449, .T. ) ;
#6127=CARTESIAN_POINT ( 'NONE',  ( -12.50000000000000000, 0.000000000000000000, 1.000000000000028644 ) ) ;
#6160=EDGE_CURVE ( 'NONE', #5938, #7303, #1530, .T. ) ;
#6290=PRODUCT_DEFINITION_SHAPE ( 'NONE', 'NONE',  #1294 ) ;
#6301=DIRECTION ( 'NONE',  ( -0.000000000000000000, -0.000000000000000000, 1.000000000000000000 ) ) ;
#6313=AXIS2_PLACEMENT_3D ( 'NONE', #1481, #4564, #7060 ) ;
#6372=ORIENTED_EDGE ( 'NONE', *, *, #1309, .F. ) ;
#6375=PLANE ( 'NONE',  #2883 ) ;
#6418=DIRECTION ( 'NONE',  ( 1.000000000000000000, 0.000000000000000000, 0.000000000000000000 ) ) ;
#6456=CARTESIAN_POINT ( 'NONE',  ( 0.000000000000000000, 0.000000000000000000, 45.00000000000000000 ) ) ;
#6625=DIRECTION ( 'NONE',  ( 0.000000000000000000, -1.000000000000000000, 0.000000000000000000 ) ) ;
#6671=CARTESIAN_POINT ( 'NONE',  ( 0.000000000000000000, 0.000000000000000000, 52.50000000000000000 ) ) ;
#6698=ADVANCED_FACE ( 'NONE', ( #3571 ), #6020, .T. ) ;
#6799=( NAMED_UNIT ( * ) PLANE_ANGLE_UNIT ( ) SI_UNIT ( $, .RADIAN. ) );
#6843=CARTESIAN_POINT ( 'NONE',  ( 0.000000000000000000, 0.000000000000000000, 45.00000000000000000 ) ) ;
#6852=CARTESIAN_POINT ( 'NONE',  ( 12.50000000000000000, 1.530808498934191127E-15, 45.00000000000000000 ) ) ;
#6863=LINE ( 'NONE', #3813, #3181 ) ;
#6882=LINE ( 'NONE', #1307, #3263 ) ;
#6889=VERTEX_POINT ( 'NONE', #4555 ) ;
#6902=CIRCLE ( 'NONE', #878, 12.50000000000000000 ) ;
#6962=DIRECTION ( 'NONE',  ( -0.7071067811865517916, 8.659560562354985860E-17, 0.7071067811865431318 ) ) ;
#6974=FACE_OUTER_BOUND ( 'NONE', #1899, .T. ) ;
#6977=DIRECTION ( 'NONE',  ( 1.000000000000000000, 0.000000000000000000, -0.000000000000000000 ) ) ;
#7014=AXIS2_PLACEMENT_3D ( 'NONE', #5739, #3775, #5123 ) ;
#7018=ORIENTED_EDGE ( 'NONE', *, *, #7145, .F. ) ;
#7060=DIRECTION ( 'NONE',  ( 1.000000000000000000, 0.000000000000000000, 0.000000000000000000 ) ) ;
#7061=DIRECTION ( 'NONE',  ( -1.000000000000000000, 0.000000000000000000, 0.000000000000000000 ) ) ;
#7123=ORIENTED_EDGE ( 'NONE', *, *, #7621, .T. ) ;
#7124=PRODUCT_DEFINITION_CONTEXT ( 'detailed design', #3731, 'design' ) ;
#7129=DIRECTION ( 'NONE',  ( 0.000000000000000000, 0.000000000000000000, 1.000000000000000000 ) ) ;
#7145=EDGE_CURVE ( 'NONE', #6889, #7297, #2934, .T. ) ;
#7202=CARTESIAN_POINT ( 'NONE',  ( 0.000000000000000000, 0.000000000000000000, 45.00000000000000000 ) ) ;
#7229=AXIS2_PLACEMENT_3D ( 'NONE', #246, #282, #6418 ) ;
#7266=VERTEX_POINT ( 'NONE', #2177 ) ;
#7297=VERTEX_POINT ( 'NONE', #4099 ) ;
#7303=VERTEX_POINT ( 'NONE', #5543 ) ;
#7309=CARTESIAN_POINT ( 'NONE',  ( 0.000000000000000000, 0.000000000000000000, 45.00000000000000000 ) ) ;
#7352=DIRECTION ( 'NONE',  ( -0.000000000000000000, -0.000000000000000000, -1.000000000000000000 ) ) ;
#7385=ADVANCED_FACE ( 'NONE', ( #5041 ), #4895, .T. ) ;
#7387=FACE_OUTER_BOUND ( 'NONE', #3567, .T. ) ;
#7435=CARTESIAN_POINT ( 'NONE',  ( 20.00000000000000000, 2.449293598294706513E-15, 52.50000000000000000 ) ) ;
#7446=CARTESIAN_POINT ( 'NONE',  ( 12.50000000000000000, 1.530808498934191127E-15, 1.000000000000028644 ) ) ;
#7449=EDGE_CURVE ( 'NONE', #3363, #243, #2032, .T. ) ;
#7533=ADVANCED_FACE ( 'NONE', ( #6974 ), #7667, .T. ) ;
#7543=DIRECTION ( 'NONE',  ( 0.000000000000000000, 0.000000000000000000, 1.000000000000000000 ) ) ;
#7549=CARTESIAN_POINT ( 'NONE',  ( 0.000000000000000000, 0.000000000000000000, 0.000000000000000000 ) ) ;
#7578=ADVANCED_FACE ( 'NONE', ( #2115 ), #4560, .T. ) ;
#7609=CIRCLE ( 'NONE', #2617, 12.50000000000000000 ) ;
#7621=EDGE_CURVE ( 'NONE', #2387, #5237, #5632, .T. ) ;
#7643=VECTOR ( 'NONE', #5015, 1000.000000000000000 ) ;
#7649=DIRECTION ( 'NONE',  ( 1.000000000000000000, 0.000000000000000000, 0.000000000000000000 ) ) ;
#7663=DIRECTION ( 'NONE',  ( -0.000000000000000000, -0.000000000000000000, -1.000000000000000000 ) ) ;
#7667=TOROIDAL_SURFACE ( 'NONE', #3192, 15.00000000000000000, 5.000000000000000000 ) ;
#7676=( NAMED_UNIT ( * ) SI_UNIT ( $, .STERADIAN. ) SOLID_ANGLE_UNIT ( ) );
#7715=DIRECTION ( 'NONE',  ( 0.000000000000000000, 0.000000000000000000, 1.000000000000000000 ) ) ;
#7777=ORIENTED_EDGE ( 'NONE', *, *, #5784, .T. ) ;
#7815=ORIENTED_EDGE ( 'NONE', *, *, #2999, .F. ) ;
#7839=VERTEX_POINT ( 'NONE', #267 ) ;
#7859=DIRECTION ( 'NONE',  ( 0.000000000000000000, 0.000000000000000000, -1.000000000000000000 ) ) ;
#7884=EDGE_CURVE ( 'NONE', #7266, #3363, #4551, .T. ) ;
#7895=ORIENTED_EDGE ( 'NONE', *, *, #3997, .F. ) ;
#7904=AXIS2_PLACEMENT_3D ( 'NONE', #5501, #1765, #1246 ) ;
#7963=COLOUR_RGB('Black',0.12,0.14,0.17);
#7964=FILL_AREA_STYLE_COLOUR('',#7963);
#7965=FILL_AREA_STYLE('',(#7964));
#7966=SURFACE_STYLE_FILL_AREA(#7965);
#7967=SURFACE_SIDE_STYLE('',(#7966));
#7968=SURFACE_STYLE_USAGE(.BOTH.,#7967);
#7969=PRESENTATION_STYLE_ASSIGNMENT((#7968));
ENDSEC;
END-ISO-10303-21;
